ISO-10303-21;
HEADER;
/* Generated by software containing ST-Developer
 * from STEP Tools, Inc. (www.steptools.com) 
 */

FILE_DESCRIPTION(
/* description */ (''),
/* implementation_level */ '2;1');

FILE_NAME(
/* name */ 'Pin_01.step',
/* time_stamp */ '2026-09-20T21:58:27+06:00',
/* author */ (''),
/* organization */ (''),
/* preprocessor_version */ 'ST-DEVELOPER v20.2',
/* originating_system */ 'Autodesk Translation Framework v15.15.0.0',
/* authorisation */ '');

FILE_SCHEMA (('AUTOMOTIVE_DESIGN { 1 0 10303 214 3 1 1 }'));
ENDSEC;

DATA;
#10=MECHANICAL_DESIGN_GEOMETRIC_PRESENTATION_REPRESENTATION('',(#60),#2238);
#44=SHAPE_REPRESENTATION_RELATIONSHIP('SRR','None',#2271,#52);
#52=ADVANCED_BREP_SHAPE_REPRESENTATION('',(#68),#2231);
#60=STYLED_ITEM('',(#2320),#68);
#68=MANIFOLD_SOLID_BREP('Pin_01',#1207);
#103=PLANE('',#1395);
#104=PLANE('',#1399);
#160=FACE_OUTER_BOUND('',#231,.T.);
#161=FACE_OUTER_BOUND('',#232,.T.);
#162=FACE_OUTER_BOUND('',#233,.T.);
#231=EDGE_LOOP('',(#1004));
#232=EDGE_LOOP('',(#1005,#1006,#1007,#1008));
#233=EDGE_LOOP('',(#1009));
#334=LINE('',#2100,#419);
#419=VECTOR('',#1714,2.25);
#493=CIRCLE('',#1396,2.25);
#494=CIRCLE('',#1398,2.25);
#591=VERTEX_POINT('',#2096);
#592=VERTEX_POINT('',#2099);
#734=EDGE_CURVE('',#591,#591,#493,.T.);
#735=EDGE_CURVE('',#591,#592,#334,.T.);
#736=EDGE_CURVE('',#592,#592,#494,.T.);
#1004=ORIENTED_EDGE('',*,*,#734,.T.);
#1005=ORIENTED_EDGE('',*,*,#734,.F.);
#1006=ORIENTED_EDGE('',*,*,#735,.T.);
#1007=ORIENTED_EDGE('',*,*,#736,.T.);
#1008=ORIENTED_EDGE('',*,*,#735,.F.);
#1009=ORIENTED_EDGE('',*,*,#736,.F.);
#1125=CYLINDRICAL_SURFACE('',#1397,2.25);
#1176=ADVANCED_FACE('',(#160),#103,.F.);
#1177=ADVANCED_FACE('',(#161),#1125,.T.);
#1178=ADVANCED_FACE('',(#162),#104,.T.);
#1207=CLOSED_SHELL('',(#1176,#1177,#1178));
#1394=AXIS2_PLACEMENT_3D('',#2094,#1706,#1707);
#1395=AXIS2_PLACEMENT_3D('',#2095,#1708,#1709);
#1396=AXIS2_PLACEMENT_3D('',#2097,#1710,#1711);
#1397=AXIS2_PLACEMENT_3D('',#2098,#1712,#1713);
#1398=AXIS2_PLACEMENT_3D('',#2101,#1715,#1716);
#1399=AXIS2_PLACEMENT_3D('',#2102,#1717,#1718);
#1706=DIRECTION('axis',(0.,0.,1.));
#1707=DIRECTION('refdir',(1.,0.,0.));
#1708=DIRECTION('center_axis',(0.,1.,0.));
#1709=DIRECTION('ref_axis',(1.,0.,0.));
#1710=DIRECTION('center_axis',(0.,-1.,0.));
#1711=DIRECTION('ref_axis',(1.,0.,0.));
#1712=DIRECTION('center_axis',(0.,-1.,0.));
#1713=DIRECTION('ref_axis',(1.,0.,0.));
#1714=DIRECTION('',(0.,1.,0.));
#1715=DIRECTION('center_axis',(0.,-1.,0.));
#1716=DIRECTION('ref_axis',(1.,0.,0.));
#1717=DIRECTION('center_axis',(0.,1.,0.));
#1718=DIRECTION('ref_axis',(1.,0.,0.));
#2094=CARTESIAN_POINT('',(0.,0.,0.));
#2095=CARTESIAN_POINT('Origin',(-17.3702842355308,-5.,34.2005167919079));
#2096=CARTESIAN_POINT('',(-19.6202842355308,-5.,34.2005167919079));
#2097=CARTESIAN_POINT('Origin',(-17.3702842355308,-5.,34.2005167919079));
#2098=CARTESIAN_POINT('Origin',(-17.3702842355308,0.,34.2005167919079));
#2099=CARTESIAN_POINT('',(-19.6202842355308,3.,34.2005167919079));
#2100=CARTESIAN_POINT('',(-19.6202842355308,0.,34.2005167919079));
#2101=CARTESIAN_POINT('Origin',(-17.3702842355308,3.,34.2005167919079));
#2102=CARTESIAN_POINT('Origin',(0.,3.,24.1717785126239));
#2221=UNCERTAINTY_MEASURE_WITH_UNIT(LENGTH_MEASURE(0.01),#2239,
'DISTANCE_ACCURACY_VALUE',
'Maximum model space distance between geometric entities at asserted c
onnectivities');
#2228=UNCERTAINTY_MEASURE_WITH_UNIT(LENGTH_MEASURE(0.01),#2239,
'DISTANCE_ACCURACY_VALUE',
'Maximum model space distance between geometric entities at asserted c
onnectivities');
#2231=(
GEOMETRIC_REPRESENTATION_CONTEXT(3)
GLOBAL_UNCERTAINTY_ASSIGNED_CONTEXT((#2221))
GLOBAL_UNIT_ASSIGNED_CONTEXT((#2239,#2241,#2242))
REPRESENTATION_CONTEXT('','3D')
);
#2238=(
GEOMETRIC_REPRESENTATION_CONTEXT(3)
GLOBAL_UNCERTAINTY_ASSIGNED_CONTEXT((#2228))
GLOBAL_UNIT_ASSIGNED_CONTEXT((#2239,#2241,#2242))
REPRESENTATION_CONTEXT('','3D')
);
#2239=(
LENGTH_UNIT()
NAMED_UNIT(*)
SI_UNIT(.MILLI.,.METRE.)
);
#2241=(
NAMED_UNIT(*)
PLANE_ANGLE_UNIT()
SI_UNIT($,.RADIAN.)
);
#2242=(
NAMED_UNIT(*)
SI_UNIT($,.STERADIAN.)
SOLID_ANGLE_UNIT()
);
#2245=SHAPE_DEFINITION_REPRESENTATION(#2254,#2271);
#2254=PRODUCT_DEFINITION_SHAPE('',$,#2281);
#2271=SHAPE_REPRESENTATION('',(#1394),#2231);
#2278=PRODUCT_DEFINITION_CONTEXT('part definition',#2307,'design');
#2281=PRODUCT_DEFINITION('Pin_01','Pin_01',#2290,#2278);
#2290=PRODUCT_DEFINITION_FORMATION('',$,#2311);
#2307=APPLICATION_CONTEXT(
'Core Data for Automotive Mechanical Design Process');
#2308=PRODUCT_CONTEXT('part definition',#2307,'mechanical');
#2311=PRODUCT('Pin_01','Pin_01',$,(#2308));
#2320=PRESENTATION_STYLE_ASSIGNMENT((#2324));
#2324=SURFACE_STYLE_USAGE(.BOTH.,#2328);
#2328=SURFACE_SIDE_STYLE('',(#2332));
#2332=SURFACE_STYLE_FILL_AREA(#2336);
#2336=FILL_AREA_STYLE('Surface - Matte',(#2340));
#2340=FILL_AREA_STYLE_COLOUR('Surface - Matte',#2344);
#2344=COLOUR_RGB('Surface - Matte', 0.66274510, 0.83137255, 0.94901961);
ENDSEC;
END-ISO-10303-21;
